ISO-10303-21;
HEADER;
FILE_DESCRIPTION (('STEP AP214'),
    '1' );
FILE_NAME ('Slewing Ring High Pressure Lip Seals Top Bottom.step',
    '2026-10-09T12:49:55',
    ( '' ),
    ( '' ),
    'SwSTEP 2.0',
    'SolidWorks 2026',
    '' );
FILE_SCHEMA (( 'AUTOMOTIVE_DESIGN' ));
ENDSEC;

DATA;
#26=EDGE_LOOP ( 'NONE', ( #5879, #12768 ) ) ;
#47=DIRECTION ( 'NONE',  ( -0.000000000000000000, 1.000000000000000000, 0.000000000000000000 ) ) ;
#76=CARTESIAN_POINT ( 'NONE',  ( 0.000000000000000000, -23.50000000000000000, 0.000000000000000000 ) ) ;
#252=EDGE_CURVE ( 'NONE', #8118, #6913, #791, .T. ) ;
#270=PLANE ( 'NONE',  #8814 ) ;
#320=VERTEX_POINT ( 'NONE', #3539 ) ;
#356=FACE_OUTER_BOUND ( 'NONE', #2990, .T. ) ;
#363=DIRECTION ( 'NONE',  ( 0.5469441386039890496, 0.000000000000000000, -0.8371691043312220470 ) ) ;
#417=ORIENTED_EDGE ( 'NONE', *, *, #10700, .F. ) ;
#420=CARTESIAN_POINT ( 'NONE',  ( 0.000000000000000000, -20.69999999999999929, 0.000000000000000000 ) ) ;
#494=DIRECTION ( 'NONE',  ( 0.5469441386039890496, 0.000000000000000000, -0.8371691043312220470 ) ) ;
#738=EDGE_CURVE ( 'NONE', #6913, #10427, #2201, .T. ) ;
#747=DIRECTION ( 'NONE',  ( 0.5469441386039890496, 0.000000000000000000, -0.8371691043312220470 ) ) ;
#791=CIRCLE ( 'NONE', #9309, 254.0000000000000000 ) ;
#805=AXIS2_PLACEMENT_3D ( 'NONE', #6711, #10765, #10635 ) ;
#831=DIRECTION ( 'NONE',  ( -0.8371691043312220470, 0.000000000000000000, -0.5469441386039890496 ) ) ;
#848=ADVANCED_FACE ( 'NONE', ( #5333, #3189 ), #270, .F. ) ;
#980=DIRECTION ( 'NONE',  ( -0.000000000000000000, 1.000000000000000000, 0.000000000000000000 ) ) ;
#998=FACE_OUTER_BOUND ( 'NONE', #9183, .T. ) ;
#1040=AXIS2_PLACEMENT_3D ( 'NONE', #2332, #3322, #7399 ) ;
#1042=CARTESIAN_POINT ( 'NONE',  ( 0.000000000000000000, -20.00000000000000000, 0.000000000000000000 ) ) ;
#1060=ADVANCED_FACE ( 'NONE', ( #3783 ), #3590, .F. ) ;
#1064=AXIS2_PLACEMENT_3D ( 'NONE', #9512, #12706, #3569 ) ;
#1118=AXIS2_PLACEMENT_3D ( 'NONE', #1698, #2559, #831 ) ;
#1260=CIRCLE ( 'NONE', #11042, 249.0000000000000284 ) ;
#1310=DIRECTION ( 'NONE',  ( -0.5024607274629890874, -0.3950277506594149224, 0.7690814609430699500 ) ) ;
#1344=LINE ( 'NONE', #2470, #2225 ) ;
#1382=ORIENTED_EDGE ( 'NONE', *, *, #10215, .T. ) ;
#1418=CARTESIAN_POINT ( 'NONE',  ( 0.000000000000000000, -25.00000000000000000, 0.000000000000000000 ) ) ;
#1493=ORIENTED_EDGE ( 'NONE', *, *, #10882, .T. ) ;
#1685=CARTESIAN_POINT ( 'NONE',  ( 0.000000000000000000, -20.00000000000000000, 0.000000000000000000 ) ) ;
#1696=CARTESIAN_POINT ( 'NONE',  ( 130.7196491263533460, -20.69999999999999929, -200.0834159351620940 ) ) ;
#1698=CARTESIAN_POINT ( 'NONE',  ( 212.6409525001303962, -22.00000000000000000, 138.9238112054132159 ) ) ;
#1713=DIRECTION ( 'NONE',  ( -0.000000000000000000, 1.000000000000000000, 0.000000000000000000 ) ) ;
#1741=CARTESIAN_POINT ( 'NONE',  ( 138.9238112054132159, -22.00000000000000000, -212.6409525001303962 ) ) ;
#1824=UNCERTAINTY_MEASURE_WITH_UNIT (LENGTH_MEASURE( 1.000000000000000082E-05 ), #12896, 'distance_accuracy_value', 'NONE');
#1854=UNCERTAINTY_MEASURE_WITH_UNIT (LENGTH_MEASURE( 1.000000000000000082E-05 ), #3560, 'distance_accuracy_value', 'NONE');
#1925=ORIENTED_EDGE ( 'NONE', *, *, #9202, .F. ) ;
#1937=VERTEX_POINT ( 'NONE', #2658 ) ;
#1988=EDGE_CURVE ( 'NONE', #10564, #320, #5546, .T. ) ;
#1994=LINE ( 'NONE', #5044, #5513 ) ;
#2004=ORIENTED_EDGE ( 'NONE', *, *, #12750, .F. ) ;
#2005=VERTEX_POINT ( 'NONE', #1741 ) ;
#2022=VERTEX_POINT ( 'NONE', #7736 ) ;
#2060=DIRECTION ( 'NONE',  ( -0.000000000000000000, 1.000000000000000000, 0.000000000000000000 ) ) ;
#2201=LINE ( 'NONE', #12405, #6580 ) ;
#2210=CARTESIAN_POINT ( 'NONE',  ( 136.1890905123932498, -22.00000000000000000, -208.4551069784743333 ) ) ;
#2225=VECTOR ( 'NONE', #5206, 1000.000000000000114 ) ;
#2281=AXIS2_PLACEMENT_3D ( 'NONE', #5729, #3855, #12860 ) ;
#2305=CARTESIAN_POINT ( 'NONE',  ( 0.000000000000000000, -20.69999999999999929, 0.000000000000000000 ) ) ;
#2332=CARTESIAN_POINT ( 'NONE',  ( 0.000000000000000000, -23.50000000000000000, 0.000000000000000000 ) ) ;
#2333=APPLICATION_CONTEXT ( 'automotive_design' ) ;
#2388=CARTESIAN_POINT ( 'NONE',  ( -138.9238112054132444, -25.00000000000000000, 212.6409525001303678 ) ) ;
#2412=DIRECTION ( 'NONE',  ( 0.5469441386039890496, 0.000000000000000000, -0.8371691043312220470 ) ) ;
#2416=CIRCLE ( 'NONE', #3254, 239.0000000000000000 ) ;
#2456=EDGE_CURVE ( 'NONE', #6913, #8118, #7451, .T. ) ;
#2459=CIRCLE ( 'NONE', #5008, 249.0000000000000284 ) ;
#2470=CARTESIAN_POINT ( 'NONE',  ( -136.1890905123932782, -22.00000000000000000, 208.4551069784743049 ) ) ;
#2488=ORIENTED_EDGE ( 'NONE', *, *, #1988, .F. ) ;
#2501=( GEOMETRIC_REPRESENTATION_CONTEXT ( 3 ) GLOBAL_UNCERTAINTY_ASSIGNED_CONTEXT ( ( #1824 ) ) GLOBAL_UNIT_ASSIGNED_CONTEXT ( ( #12896, #6905, #9095 ) ) REPRESENTATION_CONTEXT ( 'NONE', 'WORKASPACE' ) );
#2520=ORIENTED_EDGE ( 'NONE', *, *, #738, .T. ) ;
#2542=DIRECTION ( 'NONE',  ( 0.5469441386039890496, 0.000000000000000000, -0.8371691043312220470 ) ) ;
#2559=DIRECTION ( 'NONE',  ( 0.000000000000000000, -1.000000000000000000, -0.000000000000000000 ) ) ;
#2623=CARTESIAN_POINT ( 'NONE',  ( -136.1890905123932782, -22.00000000000000000, 208.4551069784743049 ) ) ;
#2658=CARTESIAN_POINT ( 'NONE',  ( 130.7196491263533460, -20.69999999999999929, -200.0834159351620940 ) ) ;
#2664=DIRECTION ( 'NONE',  ( -0.5469441386039890496, 0.000000000000000000, 0.8371691043312220470 ) ) ;
#2752=EDGE_CURVE ( 'NONE', #3580, #1937, #6425, .T. ) ;
#2804=VERTEX_POINT ( 'NONE', #5977 ) ;
#2810=DIRECTION ( 'NONE',  ( 0.5469441386039890496, 0.000000000000000000, -0.8371691043312220470 ) ) ;
#2875=PRODUCT_DEFINITION_CONTEXT ( 'detailed design', #2333, 'design' ) ;
#2967=SURFACE_STYLE_USAGE ( .BOTH. , #12377 ) ;
#2990=EDGE_LOOP ( 'NONE', ( #6155, #5771, #7768, #1493 ) ) ;
#3091=EDGE_LOOP ( 'NONE', ( #9421, #7564, #7783, #11776 ) ) ;
#3101=CARTESIAN_POINT ( 'NONE',  ( 0.000000000000000000, -22.00000000000000000, 0.000000000000000000 ) ) ;
#3117=EDGE_CURVE ( 'NONE', #1937, #8050, #12892, .T. ) ;
#3189=FACE_OUTER_BOUND ( 'NONE', #7380, .T. ) ;
#3247=COLOUR_RGB ( '', 0.09019608, 0.27058824, 0.51372549) ;
#3250=SHAPE_DEFINITION_REPRESENTATION ( #12566, #11671 ) ;
#3254=AXIS2_PLACEMENT_3D ( 'NONE', #1685, #9808, #7878 ) ;
#3322=DIRECTION ( 'NONE',  ( -0.000000000000000000, 1.000000000000000000, 0.000000000000000000 ) ) ;
#3376=EDGE_CURVE ( 'NONE', #1937, #3580, #12949, .T. ) ;
#3425=( NAMED_UNIT ( * ) PLANE_ANGLE_UNIT ( ) SI_UNIT ( $, .RADIAN. ) );
#3534=DIRECTION ( 'NONE',  ( -0.000000000000000000, 1.000000000000000000, 0.000000000000000000 ) ) ;
#3539=CARTESIAN_POINT ( 'NONE',  ( 136.1890905123932498, -22.00000000000000000, -208.4551069784743333 ) ) ;
#3560=( LENGTH_UNIT ( ) NAMED_UNIT ( * ) SI_UNIT ( .MILLI., .METRE. ) );
#3569=DIRECTION ( 'NONE',  ( 0.5469441386039890496, 0.000000000000000000, -0.8371691043312220470 ) ) ;
#3580=VERTEX_POINT ( 'NONE', #9632 ) ;
#3590=CONICAL_SURFACE ( 'NONE', #11481, 239.0000000000000000, 1.164698268477281307 ) ;
#3637=CARTESIAN_POINT ( 'NONE',  ( -130.7196491263534028, -23.50000000000000000, 200.0834159351620372 ) ) ;
#3752=DIRECTION ( 'NONE',  ( 0.000000000000000000, -1.000000000000000000, 0.000000000000000000 ) ) ;
#3783=FACE_OUTER_BOUND ( 'NONE', #3091, .T. ) ;
#3840=AXIS2_PLACEMENT_3D ( 'NONE', #9723, #3534, #747 ) ;
#3855=DIRECTION ( 'NONE',  ( -0.000000000000000000, 1.000000000000000000, 0.000000000000000000 ) ) ;
#3916=EDGE_CURVE ( 'NONE', #8050, #2022, #9905, .T. ) ;
#4080=EDGE_LOOP ( 'NONE', ( #1925, #12945, #4780, #8872 ) ) ;
#4131=DIRECTION ( 'NONE',  ( 0.5469441386039890496, 0.000000000000000000, -0.8371691043312220470 ) ) ;
#4156=AXIS2_PLACEMENT_3D ( 'NONE', #11227, #12623, #11830 ) ;
#4197=DIRECTION ( 'NONE',  ( -0.000000000000000000, 1.000000000000000000, 0.000000000000000000 ) ) ;
#4238=FILL_AREA_STYLE ('',( #9310 ) ) ;
#4329=CYLINDRICAL_SURFACE ( 'NONE', #1040, 239.0000000000000000 ) ;
#4390=DIRECTION ( 'NONE',  ( 0.000000000000000000, 1.000000000000000000, 0.000000000000000000 ) ) ;
#4403=DIRECTION ( 'NONE',  ( 0.000000000000000000, -1.000000000000000000, 0.000000000000000000 ) ) ;
#4443=AXIS2_PLACEMENT_3D ( 'NONE', #9155, #3752, #8888 ) ;
#4517=CARTESIAN_POINT ( 'NONE',  ( 0.000000000000000000, -20.69999999999999929, 0.000000000000000000 ) ) ;
#4519=STYLED_ITEM ( 'NONE', ( #7047 ), #10352 ) ;
#4646=DIRECTION ( 'NONE',  ( -0.5469441386039890496, 0.000000000000000000, 0.8371691043312220470 ) ) ;
#4652=ADVANCED_FACE ( 'NONE', ( #6136 ), #12135, .T. ) ;
#4681=EDGE_LOOP ( 'NONE', ( #2488, #9270 ) ) ;
#4780=ORIENTED_EDGE ( 'NONE', *, *, #6630, .T. ) ;
#4836=CONICAL_SURFACE ( 'NONE', #6972, 249.0000000000000284, 1.373400766945015894 ) ;
#5008=AXIS2_PLACEMENT_3D ( 'NONE', #3101, #12619, #363 ) ;
#5044=CARTESIAN_POINT ( 'NONE',  ( 138.9238112054132159, -23.50000000000000000, -212.6409525001303962 ) ) ;
#5046=CIRCLE ( 'NONE', #2281, 254.0000000000000000 ) ;
#5075=FACE_OUTER_BOUND ( 'NONE', #4080, .T. ) ;
#5118=PRODUCT_DEFINITION_FORMATION_WITH_SPECIFIED_SOURCE ( 'ANY', '', #8315, .NOT_KNOWN. ) ;
#5139=PRODUCT_DEFINITION ( 'UNKNOWN', '', #5118, #2875 ) ;
#5206=DIRECTION ( 'NONE',  ( -0.5363228529974879422, -0.1961161351381840445, 0.8209118459926720845 ) ) ;
#5209=EDGE_CURVE ( 'NONE', #2022, #8050, #1260, .T. ) ;
#5238=ADVANCED_FACE ( 'NONE', ( #5075 ), #8703, .T. ) ;
#5286=CARTESIAN_POINT ( 'NONE',  ( 0.000000000000000000, -22.00000000000000000, 0.000000000000000000 ) ) ;
#5333=FACE_BOUND ( 'NONE', #12755, .T. ) ;
#5442=CARTESIAN_POINT ( 'NONE',  ( -138.9238112054132444, -22.00000000000000000, 212.6409525001303678 ) ) ;
#5512=ADVANCED_FACE ( 'NONE', ( #356 ), #12546, .F. ) ;
#5513=VECTOR ( 'NONE', #8133, 1000.000000000000000 ) ;
#5546=CIRCLE ( 'NONE', #3840, 249.0000000000000284 ) ;
#5567=ADVANCED_FACE ( 'NONE', ( #6553 ), #8282, .F. ) ;
#5603=VECTOR ( 'NONE', #10962, 1000.000000000000000 ) ;
#5633=AXIS2_PLACEMENT_3D ( 'NONE', #6071, #2060, #7069 ) ;
#5696=FACE_OUTER_BOUND ( 'NONE', #26, .T. ) ;
#5729=CARTESIAN_POINT ( 'NONE',  ( 0.000000000000000000, -22.00000000000000000, 0.000000000000000000 ) ) ;
#5771=ORIENTED_EDGE ( 'NONE', *, *, #3376, .F. ) ;
#5868=DIRECTION ( 'NONE',  ( 0.000000000000000000, -1.000000000000000000, 0.000000000000000000 ) ) ;
#5873=CYLINDRICAL_SURFACE ( 'NONE', #5633, 254.0000000000000000 ) ;
#5879=ORIENTED_EDGE ( 'NONE', *, *, #12750, .T. ) ;
#5977=CARTESIAN_POINT ( 'NONE',  ( 130.7196491263533744, -20.00000000000000000, -200.0834159351620656 ) ) ;
#6052=DIRECTION ( 'NONE',  ( 0.5469441386039890496, 0.000000000000000000, -0.8371691043312220470 ) ) ;
#6071=CARTESIAN_POINT ( 'NONE',  ( 0.000000000000000000, -23.50000000000000000, 0.000000000000000000 ) ) ;
#6095=DIRECTION ( 'NONE',  ( -0.000000000000000000, 1.000000000000000000, 0.000000000000000000 ) ) ;
#6136=FACE_OUTER_BOUND ( 'NONE', #9101, .T. ) ;
#6144=AXIS2_PLACEMENT_3D ( 'NONE', #420, #4403, #2664 ) ;
#6155=ORIENTED_EDGE ( 'NONE', *, *, #11761, .F. ) ;
#6294=EDGE_CURVE ( 'NONE', #320, #10564, #2459, .T. ) ;
#6344=ADVANCED_BREP_SHAPE_REPRESENTATION ( '', ( #10352, #805 ), #2501 ) ;
#6414=DIRECTION ( 'NONE',  ( 0.5363228529974877201, -0.1961161351381840168, -0.8209118459926720845 ) ) ;
#6425=CIRCLE ( 'NONE', #8554, 239.0000000000000000 ) ;
#6553=FACE_OUTER_BOUND ( 'NONE', #9437, .T. ) ;
#6580=VECTOR ( 'NONE', #4197, 1000.000000000000000 ) ;
#6616=EDGE_LOOP ( 'NONE', ( #12988, #11891, #1382, #8070 ) ) ;
#6630=EDGE_CURVE ( 'NONE', #7040, #10564, #1344, .T. ) ;
#6711=CARTESIAN_POINT ( 'NONE',  ( 0.000000000000000000, 0.000000000000000000, 0.000000000000000000 ) ) ;
#6746=ADVANCED_FACE ( 'NONE', ( #998 ), #5873, .T. ) ;
#6866=DIRECTION ( 'NONE',  ( -0.5469441386039890496, 0.000000000000000000, 0.8371691043312220470 ) ) ;
#6876=( GEOMETRIC_REPRESENTATION_CONTEXT ( 3 ) GLOBAL_UNCERTAINTY_ASSIGNED_CONTEXT ( ( #1854 ) ) GLOBAL_UNIT_ASSIGNED_CONTEXT ( ( #3560, #3425, #11441 ) ) REPRESENTATION_CONTEXT ( 'NONE', 'WORKASPACE' ) );
#6905=( NAMED_UNIT ( * ) PLANE_ANGLE_UNIT ( ) SI_UNIT ( $, .RADIAN. ) );
#6913=VERTEX_POINT ( 'NONE', #2388 ) ;
#6972=AXIS2_PLACEMENT_3D ( 'NONE', #11928, #5868, #6866 ) ;
#6984=ORIENTED_EDGE ( 'NONE', *, *, #3117, .F. ) ;
#7040=VERTEX_POINT ( 'NONE', #11988 ) ;
#7047=PRESENTATION_STYLE_ASSIGNMENT (( #2967 ) ) ;
#7069=DIRECTION ( 'NONE',  ( 0.5469441386039890496, 0.000000000000000000, -0.8371691043312220470 ) ) ;
#7127=ORIENTED_EDGE ( 'NONE', *, *, #10434, .T. ) ;
#7206=AXIS2_PLACEMENT_3D ( 'NONE', #2305, #12511, #8457 ) ;
#7295=AXIS2_PLACEMENT_3D ( 'NONE', #1042, #980, #6052 ) ;
#7380=EDGE_LOOP ( 'NONE', ( #7802, #7589 ) ) ;
#7381=EDGE_CURVE ( 'NONE', #1937, #2804, #10830, .T. ) ;
#7399=DIRECTION ( 'NONE',  ( 0.5469441386039890496, 0.000000000000000000, -0.8371691043312220470 ) ) ;
#7438=VECTOR ( 'NONE', #1713, 1000.000000000000000 ) ;
#7451=CIRCLE ( 'NONE', #1064, 254.0000000000000000 ) ;
#7550=DIRECTION ( 'NONE',  ( -0.000000000000000000, 1.000000000000000000, 0.000000000000000000 ) ) ;
#7551=DIRECTION ( 'NONE',  ( -0.000000000000000000, 1.000000000000000000, 0.000000000000000000 ) ) ;
#7564=ORIENTED_EDGE ( 'NONE', *, *, #3117, .T. ) ;
#7573=CARTESIAN_POINT ( 'NONE',  ( 130.7196491263533744, -23.50000000000000000, -200.0834159351620656 ) ) ;
#7589=ORIENTED_EDGE ( 'NONE', *, *, #2456, .F. ) ;
#7651=ORIENTED_EDGE ( 'NONE', *, *, #738, .F. ) ;
#7736=CARTESIAN_POINT ( 'NONE',  ( -136.1890905123932498, -25.00000000000000000, 208.4551069784743049 ) ) ;
#7738=EDGE_LOOP ( 'NONE', ( #12149, #9553, #9506, #12431 ) ) ;
#7768=ORIENTED_EDGE ( 'NONE', *, *, #7381, .T. ) ;
#7783=ORIENTED_EDGE ( 'NONE', *, *, #5209, .F. ) ;
#7802=ORIENTED_EDGE ( 'NONE', *, *, #252, .F. ) ;
#7819=FACE_BOUND ( 'NONE', #4681, .T. ) ;
#7821=SHAPE_REPRESENTATION_RELATIONSHIP ( 'NONE' , 'NONE' ,  #11671, #6344 ) ;
#7860=FACE_OUTER_BOUND ( 'NONE', #7738, .T. ) ;
#7878=DIRECTION ( 'NONE',  ( 0.5469441386039890496, 0.000000000000000000, -0.8371691043312220470 ) ) ;
#7884=ORIENTED_EDGE ( 'NONE', *, *, #3916, .F. ) ;
#7949=CIRCLE ( 'NONE', #11145, 254.0000000000000000 ) ;
#8050=VERTEX_POINT ( 'NONE', #10908 ) ;
#8070=ORIENTED_EDGE ( 'NONE', *, *, #7381, .F. ) ;
#8118=VERTEX_POINT ( 'NONE', #11310 ) ;
#8133=DIRECTION ( 'NONE',  ( -0.000000000000000000, 1.000000000000000000, 0.000000000000000000 ) ) ;
#8164=APPLICATION_CONTEXT ( 'automotive_design' ) ;
#8282=CONICAL_SURFACE ( 'NONE', #6144, 239.0000000000000000, 1.164698268477281307 ) ;
#8315=PRODUCT ( 'Slewing Ring High Pressure Lip Seals Top Bottom', 'Slewing Ring High Pressure Lip Seals Top Bottom', '', ( #8401 ) ) ;
#8319=SURFACE_STYLE_FILL_AREA ( #4238 ) ;
#8401=PRODUCT_CONTEXT ( 'NONE', #8164, 'mechanical' ) ;
#8407=CARTESIAN_POINT ( 'NONE',  ( 212.6409525001303962, -25.00000000000000000, 138.9238112054132159 ) ) ;
#8457=DIRECTION ( 'NONE',  ( 0.5469441386039890496, 0.000000000000000000, -0.8371691043312220470 ) ) ;
#8554=AXIS2_PLACEMENT_3D ( 'NONE', #9169, #47, #12170 ) ;
#8576=LINE ( 'NONE', #12637, #9848 ) ;
#8702=DIRECTION ( 'NONE',  ( -0.000000000000000000, 1.000000000000000000, 0.000000000000000000 ) ) ;
#8703=CONICAL_SURFACE ( 'NONE', #4443, 249.0000000000000284, 1.373400766945015894 ) ;
#8814=AXIS2_PLACEMENT_3D ( 'NONE', #8407, #4390, #10467 ) ;
#8872=ORIENTED_EDGE ( 'NONE', *, *, #1988, .T. ) ;
#8888=DIRECTION ( 'NONE',  ( -0.5469441386039890496, 0.000000000000000000, 0.8371691043312220470 ) ) ;
#8898=ORIENTED_EDGE ( 'NONE', *, *, #3916, .T. ) ;
#9095=( NAMED_UNIT ( * ) SI_UNIT ( $, .STERADIAN. ) SOLID_ANGLE_UNIT ( ) );
#9101=EDGE_LOOP ( 'NONE', ( #7651, #9680, #11503, #417 ) ) ;
#9155=CARTESIAN_POINT ( 'NONE',  ( 0.000000000000000000, -22.00000000000000000, 0.000000000000000000 ) ) ;
#9169=CARTESIAN_POINT ( 'NONE',  ( 0.000000000000000000, -20.69999999999999929, 0.000000000000000000 ) ) ;
#9183=EDGE_LOOP ( 'NONE', ( #12355, #2520, #2004, #12051 ) ) ;
#9202=EDGE_CURVE ( 'NONE', #2804, #320, #10135, .T. ) ;
#9226=CLOSED_SHELL ( 'NONE', ( #12705, #11106, #1060, #6746, #9980, #4652, #848, #5567, #5512, #5238 ) ) ;
#9270=ORIENTED_EDGE ( 'NONE', *, *, #6294, .F. ) ;
#9309=AXIS2_PLACEMENT_3D ( 'NONE', #1418, #7551, #2412 ) ;
#9310=FILL_AREA_STYLE_COLOUR ( '', #3247 ) ;
#9404=FACE_OUTER_BOUND ( 'NONE', #6616, .T. ) ;
#9421=ORIENTED_EDGE ( 'NONE', *, *, #2752, .T. ) ;
#9437=EDGE_LOOP ( 'NONE', ( #6984, #11554, #7127, #7884 ) ) ;
#9506=ORIENTED_EDGE ( 'NONE', *, *, #6294, .T. ) ;
#9512=CARTESIAN_POINT ( 'NONE',  ( 0.000000000000000000, -25.00000000000000000, 0.000000000000000000 ) ) ;
#9553=ORIENTED_EDGE ( 'NONE', *, *, #9202, .T. ) ;
#9601=CARTESIAN_POINT ( 'NONE',  ( 0.000000000000000000, -23.50000000000000000, 0.000000000000000000 ) ) ;
#9632=CARTESIAN_POINT ( 'NONE',  ( -130.7196491263533744, -20.69999999999999929, 200.0834159351620656 ) ) ;
#9680=ORIENTED_EDGE ( 'NONE', *, *, #2456, .T. ) ;
#9723=CARTESIAN_POINT ( 'NONE',  ( 0.000000000000000000, -22.00000000000000000, 0.000000000000000000 ) ) ;
#9808=DIRECTION ( 'NONE',  ( -0.000000000000000000, 1.000000000000000000, 0.000000000000000000 ) ) ;
#9848=VECTOR ( 'NONE', #1310, 1000.000000000000000 ) ;
#9894=PLANE ( 'NONE',  #1118 ) ;
#9905=CIRCLE ( 'NONE', #4156, 249.0000000000000284 ) ;
#9980=ADVANCED_FACE ( 'NONE', ( #7819, #5696 ), #9894, .F. ) ;
#10135=LINE ( 'NONE', #2210, #12414 ) ;
#10215=EDGE_CURVE ( 'NONE', #7040, #2804, #10695, .T. ) ;
#10274=MECHANICAL_DESIGN_GEOMETRIC_PRESENTATION_REPRESENTATION('',(#4519),#6876);
#10325=DIRECTION ( 'NONE',  ( -0.000000000000000000, 1.000000000000000000, 0.000000000000000000 ) ) ;
#10352=MANIFOLD_SOLID_BREP ( 'NONE', #9226 ) ;
#10427=VERTEX_POINT ( 'NONE', #5442 ) ;
#10434=EDGE_CURVE ( 'NONE', #3580, #2022, #8576, .T. ) ;
#10467=DIRECTION ( 'NONE',  ( 0.5469441386039890496, 0.000000000000000000, -0.8371691043312220470 ) ) ;
#10564=VERTEX_POINT ( 'NONE', #2623 ) ;
#10635=DIRECTION ( 'NONE',  ( 1.000000000000000000, 0.000000000000000000, 0.000000000000000000 ) ) ;
#10695=CIRCLE ( 'NONE', #7295, 239.0000000000000000 ) ;
#10700=EDGE_CURVE ( 'NONE', #10427, #2005, #7949, .T. ) ;
#10765=DIRECTION ( 'NONE',  ( 0.000000000000000000, 0.000000000000000000, 1.000000000000000000 ) ) ;
#10830=LINE ( 'NONE', #7573, #11791 ) ;
#10855=DIRECTION ( 'NONE',  ( 0.000000000000000000, -1.000000000000000000, 0.000000000000000000 ) ) ;
#10882=EDGE_CURVE ( 'NONE', #2804, #7040, #2416, .T. ) ;
#10908=CARTESIAN_POINT ( 'NONE',  ( 136.1890905123932214, -25.00000000000000000, -208.4551069784743333 ) ) ;
#10962=DIRECTION ( 'NONE',  ( 0.5024607274629889764, -0.3950277506594149224, -0.7690814609430700610 ) ) ;
#11042=AXIS2_PLACEMENT_3D ( 'NONE', #11088, #6095, #2810 ) ;
#11088=CARTESIAN_POINT ( 'NONE',  ( 0.000000000000000000, -25.00000000000000000, 0.000000000000000000 ) ) ;
#11106=ADVANCED_FACE ( 'NONE', ( #9404 ), #4329, .F. ) ;
#11145=AXIS2_PLACEMENT_3D ( 'NONE', #5286, #11427, #494 ) ;
#11227=CARTESIAN_POINT ( 'NONE',  ( 0.000000000000000000, -25.00000000000000000, 0.000000000000000000 ) ) ;
#11310=CARTESIAN_POINT ( 'NONE',  ( 138.9238112054132159, -25.00000000000000000, -212.6409525001303962 ) ) ;
#11390=EDGE_CURVE ( 'NONE', #8118, #2005, #1994, .T. ) ;
#11427=DIRECTION ( 'NONE',  ( -0.000000000000000000, 1.000000000000000000, 0.000000000000000000 ) ) ;
#11441=( NAMED_UNIT ( * ) SI_UNIT ( $, .STERADIAN. ) SOLID_ANGLE_UNIT ( ) );
#11481=AXIS2_PLACEMENT_3D ( 'NONE', #4517, #10855, #4646 ) ;
#11503=ORIENTED_EDGE ( 'NONE', *, *, #11390, .T. ) ;
#11554=ORIENTED_EDGE ( 'NONE', *, *, #3376, .T. ) ;
#11671=SHAPE_REPRESENTATION ( 'Slewing Ring High Pressure Lip Seals Top Bottom', ( #805 ), #2501 ) ;
#11761=EDGE_CURVE ( 'NONE', #3580, #7040, #12907, .T. ) ;
#11765=AXIS2_PLACEMENT_3D ( 'NONE', #76, #10325, #4131 ) ;
#11776=ORIENTED_EDGE ( 'NONE', *, *, #10434, .F. ) ;
#11791=VECTOR ( 'NONE', #8702, 1000.000000000000000 ) ;
#11830=DIRECTION ( 'NONE',  ( 0.5469441386039890496, 0.000000000000000000, -0.8371691043312220470 ) ) ;
#11887=AXIS2_PLACEMENT_3D ( 'NONE', #9601, #7550, #2542 ) ;
#11891=ORIENTED_EDGE ( 'NONE', *, *, #11761, .T. ) ;
#11928=CARTESIAN_POINT ( 'NONE',  ( 0.000000000000000000, -22.00000000000000000, 0.000000000000000000 ) ) ;
#11988=CARTESIAN_POINT ( 'NONE',  ( -130.7196491263533744, -20.00000000000000000, 200.0834159351620087 ) ) ;
#12051=ORIENTED_EDGE ( 'NONE', *, *, #11390, .F. ) ;
#12135=CYLINDRICAL_SURFACE ( 'NONE', #11765, 254.0000000000000000 ) ;
#12149=ORIENTED_EDGE ( 'NONE', *, *, #10882, .F. ) ;
#12170=DIRECTION ( 'NONE',  ( 0.5469441386039890496, 0.000000000000000000, -0.8371691043312220470 ) ) ;
#12355=ORIENTED_EDGE ( 'NONE', *, *, #252, .T. ) ;
#12377=SURFACE_SIDE_STYLE ('',( #8319 ) ) ;
#12405=CARTESIAN_POINT ( 'NONE',  ( -138.9238112054132444, -23.50000000000000000, 212.6409525001303678 ) ) ;
#12414=VECTOR ( 'NONE', #6414, 1000.000000000000227 ) ;
#12431=ORIENTED_EDGE ( 'NONE', *, *, #6630, .F. ) ;
#12511=DIRECTION ( 'NONE',  ( -0.000000000000000000, 1.000000000000000000, 0.000000000000000000 ) ) ;
#12546=CYLINDRICAL_SURFACE ( 'NONE', #11887, 239.0000000000000000 ) ;
#12566=PRODUCT_DEFINITION_SHAPE ( 'NONE', 'NONE',  #5139 ) ;
#12619=DIRECTION ( 'NONE',  ( -0.000000000000000000, 1.000000000000000000, 0.000000000000000000 ) ) ;
#12623=DIRECTION ( 'NONE',  ( -0.000000000000000000, 1.000000000000000000, 0.000000000000000000 ) ) ;
#12637=CARTESIAN_POINT ( 'NONE',  ( -130.7196491263533744, -20.69999999999999929, 200.0834159351620656 ) ) ;
#12705=ADVANCED_FACE ( 'NONE', ( #7860 ), #4836, .T. ) ;
#12706=DIRECTION ( 'NONE',  ( -0.000000000000000000, 1.000000000000000000, 0.000000000000000000 ) ) ;
#12750=EDGE_CURVE ( 'NONE', #2005, #10427, #5046, .T. ) ;
#12755=EDGE_LOOP ( 'NONE', ( #12813, #8898 ) ) ;
#12768=ORIENTED_EDGE ( 'NONE', *, *, #10700, .T. ) ;
#12813=ORIENTED_EDGE ( 'NONE', *, *, #5209, .T. ) ;
#12860=DIRECTION ( 'NONE',  ( 0.5469441386039890496, 0.000000000000000000, -0.8371691043312220470 ) ) ;
#12892=LINE ( 'NONE', #1696, #5603 ) ;
#12896=( LENGTH_UNIT ( ) NAMED_UNIT ( * ) SI_UNIT ( .MILLI., .METRE. ) );
#12907=LINE ( 'NONE', #3637, #7438 ) ;
#12945=ORIENTED_EDGE ( 'NONE', *, *, #10215, .F. ) ;
#12949=CIRCLE ( 'NONE', #7206, 239.0000000000000000 ) ;
#12988=ORIENTED_EDGE ( 'NONE', *, *, #2752, .F. ) ;
ENDSEC;
END-ISO-10303-21;
